ISO-10303-21;
HEADER;
/* Generated by software containing ST-Developer
 * from STEP Tools, Inc. (www.steptools.com) 
 */

FILE_DESCRIPTION(
/* description */ ('Hinged panel with latch'),
/* implementation_level */ '2;1');

FILE_NAME(
/* name */ 'Hex Nut - M5.step',
/* time_stamp */ '2026-10-27T20:36:01-07:00',
/* author */ (''),
/* organization */ (''),
/* preprocessor_version */ 'ST-DEVELOPER v20.2',
/* originating_system */ 'Autodesk Translation Framework v15.17.0.0',
/* authorisation */ '');

FILE_SCHEMA (('AUTOMOTIVE_DESIGN { 1 0 10303 214 3 1 1 }'));
ENDSEC;

DATA;
#10=MECHANICAL_DESIGN_GEOMETRIC_PRESENTATION_REPRESENTATION('',(#310),#6743);
#219=(
BOUNDED_CURVE()
B_SPLINE_CURVE(2,(#6577,#6578,#6579),.UNSPECIFIED.,.F.,.F.)
B_SPLINE_CURVE_WITH_KNOTS((3,3),(0.140651836354967,0.670383167684795),
 .UNSPECIFIED.)
CURVE()
GEOMETRIC_REPRESENTATION_ITEM()
RATIONAL_B_SPLINE_CURVE((1.11602540378444,1.28867513459481,1.11602540378444))
REPRESENTATION_ITEM('')
);
#220=(
BOUNDED_CURVE()
B_SPLINE_CURVE(2,(#6581,#6582,#6583),.UNSPECIFIED.,.F.,.F.)
B_SPLINE_CURVE_WITH_KNOTS((3,3),(0.140651836354967,0.670383167684795),
 .UNSPECIFIED.)
CURVE()
GEOMETRIC_REPRESENTATION_ITEM()
RATIONAL_B_SPLINE_CURVE((1.11602540378444,1.28867513459481,1.11602540378444))
REPRESENTATION_ITEM('')
);
#221=(
BOUNDED_CURVE()
B_SPLINE_CURVE(2,(#6588,#6589,#6590),.UNSPECIFIED.,.F.,.F.)
B_SPLINE_CURVE_WITH_KNOTS((3,3),(0.140651836354967,0.670383167684795),
 .UNSPECIFIED.)
CURVE()
GEOMETRIC_REPRESENTATION_ITEM()
RATIONAL_B_SPLINE_CURVE((1.11602540378444,1.28867513459481,1.11602540378444))
REPRESENTATION_ITEM('')
);
#222=(
BOUNDED_CURVE()
B_SPLINE_CURVE(2,(#6592,#6593,#6594),.UNSPECIFIED.,.F.,.F.)
B_SPLINE_CURVE_WITH_KNOTS((3,3),(0.140651836354967,0.670383167684795),
 .UNSPECIFIED.)
CURVE()
GEOMETRIC_REPRESENTATION_ITEM()
RATIONAL_B_SPLINE_CURVE((1.11602540378444,1.28867513459481,1.11602540378444))
REPRESENTATION_ITEM('')
);
#223=(
BOUNDED_CURVE()
B_SPLINE_CURVE(2,(#6596,#6597,#6598),.UNSPECIFIED.,.F.,.F.)
B_SPLINE_CURVE_WITH_KNOTS((3,3),(0.140651836354967,0.670383167684795),
 .UNSPECIFIED.)
CURVE()
GEOMETRIC_REPRESENTATION_ITEM()
RATIONAL_B_SPLINE_CURVE((1.11602540378444,1.28867513459481,1.11602540378444))
REPRESENTATION_ITEM('')
);
#224=(
BOUNDED_CURVE()
B_SPLINE_CURVE(2,(#6599,#6600,#6601),.UNSPECIFIED.,.F.,.F.)
B_SPLINE_CURVE_WITH_KNOTS((3,3),(0.140651836354967,0.670383167684795),
 .UNSPECIFIED.)
CURVE()
GEOMETRIC_REPRESENTATION_ITEM()
RATIONAL_B_SPLINE_CURVE((1.11602540378444,1.28867513459481,1.11602540378444))
REPRESENTATION_ITEM('')
);
#225=(
BOUNDED_CURVE()
B_SPLINE_CURVE(2,(#6608,#6609,#6610),.UNSPECIFIED.,.F.,.F.)
B_SPLINE_CURVE_WITH_KNOTS((3,3),(0.140651836354967,0.670383167684795),
 .UNSPECIFIED.)
CURVE()
GEOMETRIC_REPRESENTATION_ITEM()
RATIONAL_B_SPLINE_CURVE((1.11602540378444,1.28867513459481,1.11602540378444))
REPRESENTATION_ITEM('')
);
#226=(
BOUNDED_CURVE()
B_SPLINE_CURVE(2,(#6612,#6613,#6614),.UNSPECIFIED.,.F.,.F.)
B_SPLINE_CURVE_WITH_KNOTS((3,3),(0.140651836354967,0.670383167684796),
 .UNSPECIFIED.)
CURVE()
GEOMETRIC_REPRESENTATION_ITEM()
RATIONAL_B_SPLINE_CURVE((1.11602540378444,1.28867513459481,1.11602540378444))
REPRESENTATION_ITEM('')
);
#227=(
BOUNDED_CURVE()
B_SPLINE_CURVE(2,(#6616,#6617,#6618),.UNSPECIFIED.,.F.,.F.)
B_SPLINE_CURVE_WITH_KNOTS((3,3),(0.140651836354967,0.670383167684795),
 .UNSPECIFIED.)
CURVE()
GEOMETRIC_REPRESENTATION_ITEM()
RATIONAL_B_SPLINE_CURVE((1.11602540378444,1.28867513459481,1.11602540378444))
REPRESENTATION_ITEM('')
);
#228=(
BOUNDED_CURVE()
B_SPLINE_CURVE(2,(#6620,#6621,#6622),.UNSPECIFIED.,.F.,.F.)
B_SPLINE_CURVE_WITH_KNOTS((3,3),(0.140651836354967,0.670383167684795),
 .UNSPECIFIED.)
CURVE()
GEOMETRIC_REPRESENTATION_ITEM()
RATIONAL_B_SPLINE_CURVE((1.11602540378444,1.28867513459482,1.11602540378444))
REPRESENTATION_ITEM('')
);
#229=(
BOUNDED_CURVE()
B_SPLINE_CURVE(2,(#6624,#6625,#6626),.UNSPECIFIED.,.F.,.F.)
B_SPLINE_CURVE_WITH_KNOTS((3,3),(0.140651836354967,0.670383167684795),
 .UNSPECIFIED.)
CURVE()
GEOMETRIC_REPRESENTATION_ITEM()
RATIONAL_B_SPLINE_CURVE((1.11602540378444,1.28867513459481,1.11602540378444))
REPRESENTATION_ITEM('')
);
#230=(
BOUNDED_CURVE()
B_SPLINE_CURVE(2,(#6627,#6628,#6629),.UNSPECIFIED.,.F.,.F.)
B_SPLINE_CURVE_WITH_KNOTS((3,3),(0.140651836354967,0.670383167684795),
 .UNSPECIFIED.)
CURVE()
GEOMETRIC_REPRESENTATION_ITEM()
RATIONAL_B_SPLINE_CURVE((1.11602540378444,1.28867513459481,1.11602540378444))
REPRESENTATION_ITEM('')
);
#256=CONICAL_SURFACE('',#4320,0.47094010767585,1.0471975511966);
#257=CONICAL_SURFACE('',#4322,0.47094010767585,1.0471975511966);
#278=SHAPE_REPRESENTATION_RELATIONSHIP('SRR','None',#6854,#294);
#294=ADVANCED_BREP_SHAPE_REPRESENTATION('',(#323),#6740);
#310=STYLED_ITEM('',(#7010),#323);
#323=MANIFOLD_SOLID_BREP('Body1',#3815);
#368=FACE_BOUND('',#970,.T.);
#369=FACE_BOUND('',#972,.T.);
#509=PLANE('',#4324);
#510=PLANE('',#4325);
#511=PLANE('',#4326);
#512=PLANE('',#4330);
#513=PLANE('',#4331);
#514=PLANE('',#4332);
#515=PLANE('',#4333);
#516=PLANE('',#4334);
#711=FACE_OUTER_BOUND('',#960,.T.);
#712=FACE_OUTER_BOUND('',#961,.T.);
#713=FACE_OUTER_BOUND('',#962,.T.);
#714=FACE_OUTER_BOUND('',#963,.T.);
#715=FACE_OUTER_BOUND('',#964,.T.);
#716=FACE_OUTER_BOUND('',#965,.T.);
#717=FACE_OUTER_BOUND('',#966,.T.);
#718=FACE_OUTER_BOUND('',#967,.T.);
#719=FACE_OUTER_BOUND('',#968,.T.);
#720=FACE_OUTER_BOUND('',#969,.T.);
#721=FACE_OUTER_BOUND('',#971,.T.);
#960=EDGE_LOOP('',(#3476,#3477,#3478,#3479,#3480,#3481,#3482,#3483,#3484));
#961=EDGE_LOOP('',(#3485,#3486,#3487,#3488,#3489,#3490,#3491,#3492,#3493));
#962=EDGE_LOOP('',(#3494,#3495,#3496,#3497));
#963=EDGE_LOOP('',(#3498,#3499,#3500,#3501));
#964=EDGE_LOOP('',(#3502,#3503,#3504,#3505));
#965=EDGE_LOOP('',(#3506,#3507,#3508,#3509));
#966=EDGE_LOOP('',(#3510,#3511,#3512,#3513));
#967=EDGE_LOOP('',(#3514,#3515,#3516,#3517));
#968=EDGE_LOOP('',(#3518,#3519,#3520,#3521));
#969=EDGE_LOOP('',(#3522));
#970=EDGE_LOOP('',(#3523));
#971=EDGE_LOOP('',(#3524));
#972=EDGE_LOOP('',(#3525));
#1318=LINE('',#6585,#1676);
#1319=LINE('',#6606,#1677);
#1320=LINE('',#6631,#1678);
#1321=LINE('',#6632,#1679);
#1322=LINE('',#6634,#1680);
#1323=LINE('',#6636,#1681);
#1324=LINE('',#6641,#1682);
#1325=LINE('',#6644,#1683);
#1326=LINE('',#6646,#1684);
#1676=VECTOR('',#5354,0.47094010767585);
#1677=VECTOR('',#5361,0.47094010767585);
#1678=VECTOR('',#5364,1.);
#1679=VECTOR('',#5365,1.);
#1680=VECTOR('',#5368,1.);
#1681=VECTOR('',#5371,1.);
#1682=VECTOR('',#5376,0.25);
#1683=VECTOR('',#5381,1.);
#1684=VECTOR('',#5384,1.);
#1785=CIRCLE('',#4321,0.38);
#1786=CIRCLE('',#4323,0.38);
#1787=CIRCLE('',#4328,0.2117);
#1788=CIRCLE('',#4329,0.2117);
#2081=VERTEX_POINT('',#6575);
#2082=VERTEX_POINT('',#6576);
#2083=VERTEX_POINT('',#6580);
#2084=VERTEX_POINT('',#6584);
#2085=VERTEX_POINT('',#6587);
#2086=VERTEX_POINT('',#6591);
#2087=VERTEX_POINT('',#6595);
#2088=VERTEX_POINT('',#6603);
#2089=VERTEX_POINT('',#6605);
#2090=VERTEX_POINT('',#6607);
#2091=VERTEX_POINT('',#6611);
#2092=VERTEX_POINT('',#6615);
#2093=VERTEX_POINT('',#6619);
#2094=VERTEX_POINT('',#6623);
#2095=VERTEX_POINT('',#6638);
#2096=VERTEX_POINT('',#6640);
#2550=EDGE_CURVE('',#2081,#2082,#219,.T.);
#2551=EDGE_CURVE('',#2083,#2081,#220,.T.);
#2552=EDGE_CURVE('',#2083,#2084,#1318,.T.);
#2553=EDGE_CURVE('',#2084,#2084,#1785,.T.);
#2554=EDGE_CURVE('',#2085,#2083,#221,.T.);
#2555=EDGE_CURVE('',#2086,#2085,#222,.T.);
#2556=EDGE_CURVE('',#2087,#2086,#223,.T.);
#2557=EDGE_CURVE('',#2082,#2087,#224,.T.);
#2558=EDGE_CURVE('',#2088,#2088,#1786,.T.);
#2559=EDGE_CURVE('',#2088,#2089,#1319,.T.);
#2560=EDGE_CURVE('',#2090,#2089,#225,.T.);
#2561=EDGE_CURVE('',#2091,#2090,#226,.T.);
#2562=EDGE_CURVE('',#2092,#2091,#227,.T.);
#2563=EDGE_CURVE('',#2093,#2092,#228,.T.);
#2564=EDGE_CURVE('',#2094,#2093,#229,.T.);
#2565=EDGE_CURVE('',#2089,#2094,#230,.T.);
#2566=EDGE_CURVE('',#2085,#2094,#1320,.T.);
#2567=EDGE_CURVE('',#2086,#2093,#1321,.T.);
#2568=EDGE_CURVE('',#2083,#2089,#1322,.T.);
#2569=EDGE_CURVE('',#2081,#2090,#1323,.T.);
#2570=EDGE_CURVE('',#2095,#2095,#1787,.F.);
#2571=EDGE_CURVE('',#2095,#2096,#1324,.T.);
#2572=EDGE_CURVE('',#2096,#2096,#1788,.F.);
#2573=EDGE_CURVE('',#2082,#2091,#1325,.T.);
#2574=EDGE_CURVE('',#2087,#2092,#1326,.T.);
#3476=ORIENTED_EDGE('',*,*,#2550,.F.);
#3477=ORIENTED_EDGE('',*,*,#2551,.F.);
#3478=ORIENTED_EDGE('',*,*,#2552,.T.);
#3479=ORIENTED_EDGE('',*,*,#2553,.F.);
#3480=ORIENTED_EDGE('',*,*,#2552,.F.);
#3481=ORIENTED_EDGE('',*,*,#2554,.F.);
#3482=ORIENTED_EDGE('',*,*,#2555,.F.);
#3483=ORIENTED_EDGE('',*,*,#2556,.F.);
#3484=ORIENTED_EDGE('',*,*,#2557,.F.);
#3485=ORIENTED_EDGE('',*,*,#2558,.F.);
#3486=ORIENTED_EDGE('',*,*,#2559,.T.);
#3487=ORIENTED_EDGE('',*,*,#2560,.F.);
#3488=ORIENTED_EDGE('',*,*,#2561,.F.);
#3489=ORIENTED_EDGE('',*,*,#2562,.F.);
#3490=ORIENTED_EDGE('',*,*,#2563,.F.);
#3491=ORIENTED_EDGE('',*,*,#2564,.F.);
#3492=ORIENTED_EDGE('',*,*,#2565,.F.);
#3493=ORIENTED_EDGE('',*,*,#2559,.F.);
#3494=ORIENTED_EDGE('',*,*,#2555,.T.);
#3495=ORIENTED_EDGE('',*,*,#2566,.T.);
#3496=ORIENTED_EDGE('',*,*,#2564,.T.);
#3497=ORIENTED_EDGE('',*,*,#2567,.F.);
#3498=ORIENTED_EDGE('',*,*,#2554,.T.);
#3499=ORIENTED_EDGE('',*,*,#2568,.T.);
#3500=ORIENTED_EDGE('',*,*,#2565,.T.);
#3501=ORIENTED_EDGE('',*,*,#2566,.F.);
#3502=ORIENTED_EDGE('',*,*,#2551,.T.);
#3503=ORIENTED_EDGE('',*,*,#2569,.T.);
#3504=ORIENTED_EDGE('',*,*,#2560,.T.);
#3505=ORIENTED_EDGE('',*,*,#2568,.F.);
#3506=ORIENTED_EDGE('',*,*,#2570,.F.);
#3507=ORIENTED_EDGE('',*,*,#2571,.T.);
#3508=ORIENTED_EDGE('',*,*,#2572,.T.);
#3509=ORIENTED_EDGE('',*,*,#2571,.F.);
#3510=ORIENTED_EDGE('',*,*,#2550,.T.);
#3511=ORIENTED_EDGE('',*,*,#2573,.T.);
#3512=ORIENTED_EDGE('',*,*,#2561,.T.);
#3513=ORIENTED_EDGE('',*,*,#2569,.F.);
#3514=ORIENTED_EDGE('',*,*,#2556,.T.);
#3515=ORIENTED_EDGE('',*,*,#2567,.T.);
#3516=ORIENTED_EDGE('',*,*,#2563,.T.);
#3517=ORIENTED_EDGE('',*,*,#2574,.F.);
#3518=ORIENTED_EDGE('',*,*,#2557,.T.);
#3519=ORIENTED_EDGE('',*,*,#2574,.T.);
#3520=ORIENTED_EDGE('',*,*,#2562,.T.);
#3521=ORIENTED_EDGE('',*,*,#2573,.F.);
#3522=ORIENTED_EDGE('',*,*,#2558,.T.);
#3523=ORIENTED_EDGE('',*,*,#2570,.T.);
#3524=ORIENTED_EDGE('',*,*,#2553,.T.);
#3525=ORIENTED_EDGE('',*,*,#2572,.F.);
#3590=CYLINDRICAL_SURFACE('',#4327,0.2117);
#3780=ADVANCED_FACE('',(#711),#256,.T.);
#3781=ADVANCED_FACE('',(#712),#257,.T.);
#3782=ADVANCED_FACE('',(#713),#509,.T.);
#3783=ADVANCED_FACE('',(#714),#510,.T.);
#3784=ADVANCED_FACE('',(#715),#511,.T.);
#3785=ADVANCED_FACE('',(#716),#3590,.F.);
#3786=ADVANCED_FACE('',(#717),#512,.T.);
#3787=ADVANCED_FACE('',(#718),#513,.T.);
#3788=ADVANCED_FACE('',(#719),#514,.T.);
#3789=ADVANCED_FACE('',(#720,#368),#515,.T.);
#3790=ADVANCED_FACE('',(#721,#369),#516,.F.);
#3815=CLOSED_SHELL('',(#3780,#3781,#3782,#3783,#3784,#3785,#3786,#3787,
#3788,#3789,#3790));
#4319=AXIS2_PLACEMENT_3D('',#6573,#5350,#5351);
#4320=AXIS2_PLACEMENT_3D('',#6574,#5352,#5353);
#4321=AXIS2_PLACEMENT_3D('',#6586,#5355,#5356);
#4322=AXIS2_PLACEMENT_3D('',#6602,#5357,#5358);
#4323=AXIS2_PLACEMENT_3D('',#6604,#5359,#5360);
#4324=AXIS2_PLACEMENT_3D('',#6630,#5362,#5363);
#4325=AXIS2_PLACEMENT_3D('',#6633,#5366,#5367);
#4326=AXIS2_PLACEMENT_3D('',#6635,#5369,#5370);
#4327=AXIS2_PLACEMENT_3D('',#6637,#5372,#5373);
#4328=AXIS2_PLACEMENT_3D('',#6639,#5374,#5375);
#4329=AXIS2_PLACEMENT_3D('',#6642,#5377,#5378);
#4330=AXIS2_PLACEMENT_3D('',#6643,#5379,#5380);
#4331=AXIS2_PLACEMENT_3D('',#6645,#5382,#5383);
#4332=AXIS2_PLACEMENT_3D('',#6647,#5385,#5386);
#4333=AXIS2_PLACEMENT_3D('',#6648,#5387,#5388);
#4334=AXIS2_PLACEMENT_3D('',#6649,#5389,#5390);
#5350=DIRECTION('axis',(0.,0.,1.));
#5351=DIRECTION('refdir',(1.,0.,0.));
#5352=DIRECTION('center_axis',(0.,1.,0.));
#5353=DIRECTION('ref_axis',(1.,0.,0.));
#5354=DIRECTION('',(0.866025403784439,-0.5,1.06057523872491E-16));
#5355=DIRECTION('center_axis',(0.,-1.,0.));
#5356=DIRECTION('ref_axis',(1.,0.,0.));
#5357=DIRECTION('center_axis',(0.,-1.,0.));
#5358=DIRECTION('ref_axis',(1.,0.,0.));
#5359=DIRECTION('center_axis',(0.,1.,0.));
#5360=DIRECTION('ref_axis',(1.,0.,0.));
#5361=DIRECTION('',(-0.866025403784439,-0.5,-1.06057523872491E-16));
#5362=DIRECTION('center_axis',(1.20185167898973E-16,0.,-1.));
#5363=DIRECTION('ref_axis',(-1.,0.,-1.20185167898973E-16));
#5364=DIRECTION('',(0.,1.,0.));
#5365=DIRECTION('',(0.,1.,0.));
#5366=DIRECTION('center_axis',(-0.866025403784439,0.,-0.5));
#5367=DIRECTION('ref_axis',(-0.5,0.,0.866025403784439));
#5368=DIRECTION('',(0.,1.,0.));
#5369=DIRECTION('center_axis',(-0.866025403784439,0.,0.5));
#5370=DIRECTION('ref_axis',(0.5,0.,0.866025403784439));
#5371=DIRECTION('',(0.,1.,0.));
#5372=DIRECTION('center_axis',(0.,1.,0.));
#5373=DIRECTION('ref_axis',(1.,0.,0.));
#5374=DIRECTION('center_axis',(0.,1.,0.));
#5375=DIRECTION('ref_axis',(1.,0.,0.));
#5376=DIRECTION('',(0.,-1.,0.));
#5377=DIRECTION('center_axis',(0.,1.,0.));
#5378=DIRECTION('ref_axis',(1.,0.,0.));
#5379=DIRECTION('center_axis',(-2.40370335797945E-16,0.,1.));
#5380=DIRECTION('ref_axis',(1.,0.,2.40370335797945E-16));
#5381=DIRECTION('',(0.,1.,0.));
#5382=DIRECTION('center_axis',(0.866025403784439,0.,-0.5));
#5383=DIRECTION('ref_axis',(-0.5,0.,-0.866025403784439));
#5384=DIRECTION('',(0.,1.,0.));
#5385=DIRECTION('center_axis',(0.866025403784439,0.,0.5));
#5386=DIRECTION('ref_axis',(0.5,0.,-0.866025403784439));
#5387=DIRECTION('center_axis',(0.,1.,0.));
#5388=DIRECTION('ref_axis',(1.,0.,0.));
#5389=DIRECTION('center_axis',(0.,1.,0.));
#5390=DIRECTION('ref_axis',(1.,0.,0.));
#6573=CARTESIAN_POINT('',(0.,0.,0.));
#6574=CARTESIAN_POINT('Origin',(0.,0.0525042956467857,0.));
#6575=CARTESIAN_POINT('',(-0.230940107675851,0.0472735643746089,0.4));
#6576=CARTESIAN_POINT('',(0.23094010767585,0.0472735643746089,0.4));
#6577=CARTESIAN_POINT('Ctrl Pts',(-0.230940107675851,0.0472735643746089,
0.4));
#6578=CARTESIAN_POINT('Ctrl Pts',(1.11022302462516E-16,-0.0193931022920578,
0.4));
#6579=CARTESIAN_POINT('Ctrl Pts',(0.23094010767585,0.0472735643746089,0.4));
#6580=CARTESIAN_POINT('',(-0.461880215351701,0.0472735643746089,-5.6564012731995E-17));
#6581=CARTESIAN_POINT('Ctrl Pts',(-0.461880215351701,0.0472735643746089,
-5.6564012731995E-17));
#6582=CARTESIAN_POINT('Ctrl Pts',(-0.346410161513776,-0.0193931022920579,
0.2));
#6583=CARTESIAN_POINT('Ctrl Pts',(-0.230940107675851,0.0472735643746089,
0.4));
#6584=CARTESIAN_POINT('',(-0.38,-2.08166817117217E-17,-4.65365783675994E-17));
#6585=CARTESIAN_POINT('',(-0.47094010767585,0.0525042956467857,-5.7673529545534E-17));
#6586=CARTESIAN_POINT('Origin',(0.,0.,0.));
#6587=CARTESIAN_POINT('',(-0.23094010767585,0.0472735643746089,-0.4));
#6588=CARTESIAN_POINT('Ctrl Pts',(-0.23094010767585,0.0472735643746089,
-0.4));
#6589=CARTESIAN_POINT('Ctrl Pts',(-0.346410161513775,-0.0193931022920578,
-0.2));
#6590=CARTESIAN_POINT('Ctrl Pts',(-0.461880215351701,0.0472735643746089,
-5.6564012731995E-17));
#6591=CARTESIAN_POINT('',(0.23094010767585,0.0472735643746089,-0.4));
#6592=CARTESIAN_POINT('Ctrl Pts',(0.23094010767585,0.0472735643746089,-0.4));
#6593=CARTESIAN_POINT('Ctrl Pts',(0.,-0.0193931022920578,-0.4));
#6594=CARTESIAN_POINT('Ctrl Pts',(-0.23094010767585,0.0472735643746089,
-0.4));
#6595=CARTESIAN_POINT('',(0.461880215351701,0.0472735643746089,0.));
#6596=CARTESIAN_POINT('Ctrl Pts',(0.461880215351701,0.0472735643746089,
0.));
#6597=CARTESIAN_POINT('Ctrl Pts',(0.346410161513776,-0.019393102292058,
-0.2));
#6598=CARTESIAN_POINT('Ctrl Pts',(0.23094010767585,0.0472735643746089,-0.4));
#6599=CARTESIAN_POINT('Ctrl Pts',(0.23094010767585,0.0472735643746089,0.4));
#6600=CARTESIAN_POINT('Ctrl Pts',(0.346410161513776,-0.0193931022920577,
0.2));
#6601=CARTESIAN_POINT('Ctrl Pts',(0.461880215351701,0.0472735643746089,
0.));
#6602=CARTESIAN_POINT('Origin',(0.,0.417495704353214,0.));
#6603=CARTESIAN_POINT('',(-0.38,0.47,-4.65365783675994E-17));
#6604=CARTESIAN_POINT('Origin',(0.,0.47,0.));
#6605=CARTESIAN_POINT('',(-0.461880215351701,0.422726435625391,-5.6564012731995E-17));
#6606=CARTESIAN_POINT('',(-0.47094010767585,0.417495704353214,-5.7673529545534E-17));
#6607=CARTESIAN_POINT('',(-0.230940107675851,0.422726435625391,0.4));
#6608=CARTESIAN_POINT('Ctrl Pts',(-0.230940107675851,0.422726435625391,
0.4));
#6609=CARTESIAN_POINT('Ctrl Pts',(-0.346410161513776,0.489393102292058,
0.2));
#6610=CARTESIAN_POINT('Ctrl Pts',(-0.461880215351701,0.422726435625391,
-5.6564012731995E-17));
#6611=CARTESIAN_POINT('',(0.23094010767585,0.422726435625391,0.4));
#6612=CARTESIAN_POINT('Ctrl Pts',(0.23094010767585,0.422726435625391,0.4));
#6613=CARTESIAN_POINT('Ctrl Pts',(8.32667268468867E-17,0.489393102292058,
0.4));
#6614=CARTESIAN_POINT('Ctrl Pts',(-0.230940107675851,0.422726435625391,
0.4));
#6615=CARTESIAN_POINT('',(0.461880215351701,0.422726435625391,0.));
#6616=CARTESIAN_POINT('Ctrl Pts',(0.461880215351701,0.422726435625391,0.));
#6617=CARTESIAN_POINT('Ctrl Pts',(0.346410161513776,0.489393102292058,0.2));
#6618=CARTESIAN_POINT('Ctrl Pts',(0.23094010767585,0.422726435625391,0.4));
#6619=CARTESIAN_POINT('',(0.23094010767585,0.422726435625391,-0.4));
#6620=CARTESIAN_POINT('Ctrl Pts',(0.23094010767585,0.422726435625391,-0.4));
#6621=CARTESIAN_POINT('Ctrl Pts',(0.346410161513775,0.489393102292058,-0.2));
#6622=CARTESIAN_POINT('Ctrl Pts',(0.461880215351701,0.422726435625391,0.));
#6623=CARTESIAN_POINT('',(-0.23094010767585,0.422726435625391,-0.4));
#6624=CARTESIAN_POINT('Ctrl Pts',(-0.23094010767585,0.422726435625391,-0.4));
#6625=CARTESIAN_POINT('Ctrl Pts',(-5.55111512312578E-17,0.489393102292058,
-0.4));
#6626=CARTESIAN_POINT('Ctrl Pts',(0.23094010767585,0.422726435625391,-0.4));
#6627=CARTESIAN_POINT('Ctrl Pts',(-0.461880215351701,0.422726435625391,
-5.6564012731995E-17));
#6628=CARTESIAN_POINT('Ctrl Pts',(-0.346410161513776,0.489393102292058,
-0.2));
#6629=CARTESIAN_POINT('Ctrl Pts',(-0.23094010767585,0.422726435625391,-0.4));
#6630=CARTESIAN_POINT('Origin',(0.23094010767585,0.,-0.4));
#6631=CARTESIAN_POINT('',(-0.23094010767585,0.,-0.4));
#6632=CARTESIAN_POINT('',(0.23094010767585,0.,-0.4));
#6633=CARTESIAN_POINT('Origin',(-0.23094010767585,0.,-0.4));
#6634=CARTESIAN_POINT('',(-0.461880215351701,0.,-5.6564012731995E-17));
#6635=CARTESIAN_POINT('Origin',(-0.461880215351701,0.,-5.6564012731995E-17));
#6636=CARTESIAN_POINT('',(-0.230940107675851,0.,0.4));
#6637=CARTESIAN_POINT('Origin',(0.,0.,0.));
#6638=CARTESIAN_POINT('',(-0.2117,0.47,2.59257727379495E-17));
#6639=CARTESIAN_POINT('Origin',(0.,0.47,0.));
#6640=CARTESIAN_POINT('',(-0.2117,0.,2.59257727379495E-17));
#6641=CARTESIAN_POINT('',(-0.2117,0.,2.59257727379495E-17));
#6642=CARTESIAN_POINT('Origin',(0.,0.,0.));
#6643=CARTESIAN_POINT('Origin',(-0.230940107675851,0.,0.4));
#6644=CARTESIAN_POINT('',(0.23094010767585,0.,0.4));
#6645=CARTESIAN_POINT('Origin',(0.461880215351701,0.,0.));
#6646=CARTESIAN_POINT('',(0.461880215351701,0.,0.));
#6647=CARTESIAN_POINT('Origin',(0.23094010767585,0.,0.4));
#6648=CARTESIAN_POINT('Origin',(0.,0.47,0.));
#6649=CARTESIAN_POINT('Origin',(0.,0.,0.));
#6719=UNCERTAINTY_MEASURE_WITH_UNIT(LENGTH_MEASURE(0.001),#6744,
'DISTANCE_ACCURACY_VALUE',
'Maximum model space distance between geometric entities at asserted c
onnectivities');
#6722=UNCERTAINTY_MEASURE_WITH_UNIT(LENGTH_MEASURE(0.001),#6744,
'DISTANCE_ACCURACY_VALUE',
'Maximum model space distance between geometric entities at asserted c
onnectivities');
#6740=(
GEOMETRIC_REPRESENTATION_CONTEXT(3)
GLOBAL_UNCERTAINTY_ASSIGNED_CONTEXT((#6719))
GLOBAL_UNIT_ASSIGNED_CONTEXT((#6744,#6746,#6747))
REPRESENTATION_CONTEXT('','3D')
);
#6743=(
GEOMETRIC_REPRESENTATION_CONTEXT(3)
GLOBAL_UNCERTAINTY_ASSIGNED_CONTEXT((#6722))
GLOBAL_UNIT_ASSIGNED_CONTEXT((#6744,#6746,#6747))
REPRESENTATION_CONTEXT('','3D')
);
#6744=(
LENGTH_UNIT()
NAMED_UNIT(*)
SI_UNIT(.CENTI.,.METRE.)
);
#6746=(
NAMED_UNIT(*)
PLANE_ANGLE_UNIT()
SI_UNIT($,.RADIAN.)
);
#6747=(
NAMED_UNIT(*)
SI_UNIT($,.STERADIAN.)
SOLID_ANGLE_UNIT()
);
#6765=SHAPE_DEFINITION_REPRESENTATION(#6816,#6854);
#6816=PRODUCT_DEFINITION_SHAPE('',$,#6875);
#6854=SHAPE_REPRESENTATION('',(#4319),#6740);
#6857=PRODUCT_DEFINITION_CONTEXT('part definition',#6919,'design');
#6875=PRODUCT_DEFINITION('Hex Nut - M5','Hex Nut - M5',#6895,#6857);
#6895=PRODUCT_DEFINITION_FORMATION('',$,#6938);
#6919=APPLICATION_CONTEXT(
'Core Data for Automotive Mechanical Design Process');
#6920=PRODUCT_CONTEXT('part definition',#6919,'mechanical');
#6938=PRODUCT('Hex Nut - M5','Hex Nut - M5','Hex Nut - M5',(#6920));
#7004=COLOUR_RGB('Black',0.12,0.14,0.17);
#7005=FILL_AREA_STYLE_COLOUR('',#7004);
#7006=FILL_AREA_STYLE('',(#7005));
#7007=SURFACE_STYLE_FILL_AREA(#7006);
#7008=SURFACE_SIDE_STYLE('',(#7007));
#7009=SURFACE_STYLE_USAGE(.BOTH.,#7008);
#7010=PRESENTATION_STYLE_ASSIGNMENT((#7009));
ENDSEC;
END-ISO-10303-21;
